ISO-10303-21;
HEADER;
/* Generated by software containing ST-Developer
 * from STEP Tools, Inc. (www.steptools.com) 
 */

FILE_DESCRIPTION(
/* description */ ('STEP AP214'),
/* implementation_level */ '2;1');

FILE_NAME(
/* name */ 'Button Head Cap Screw M4x0.7x4.step',
/* time_stamp */ '2026-11-14T22:03:06-08:00',
/* author */ (''),
/* organization */ (''),
/* preprocessor_version */ 'ST-DEVELOPER v20.2',
/* originating_system */ 'Autodesk Translation Framework v15.17.0.0',
/* authorisation */ '');

FILE_SCHEMA (('AUTOMOTIVE_DESIGN { 1 0 10303 214 3 1 1 }'));
ENDSEC;

DATA;
#10=MECHANICAL_DESIGN_GEOMETRIC_PRESENTATION_REPRESENTATION('',(#313),#12966);
#153=SPHERICAL_SURFACE('',#6134,4.3249693283142);
#157=TOROIDAL_SURFACE('',#6123,2.2,0.2);
#163=CONICAL_SURFACE('',#6116,1732.05080756886,1.04719755119659);
#164=CONICAL_SURFACE('',#6127,1.61,0.785398163397447);
#293=SHAPE_REPRESENTATION_RELATIONSHIP('SRR','None',#13031,#301);
#301=ADVANCED_BREP_SHAPE_REPRESENTATION('',(#325),#12964);
#313=STYLED_ITEM('',(#13075),#325);
#325=MANIFOLD_SOLID_BREP('Body1',#5588);
#383=FACE_BOUND('',#1192,.T.);
#384=FACE_BOUND('',#1194,.T.);
#385=FACE_BOUND('',#1196,.T.);
#520=PLANE('',#6136);
#521=PLANE('',#6137);
#522=PLANE('',#6138);
#523=PLANE('',#6139);
#524=PLANE('',#6140);
#525=PLANE('',#6141);
#526=PLANE('',#6142);
#527=PLANE('',#6143);
#528=PLANE('',#6144);
#529=PLANE('',#6145);
#530=PLANE('',#6146);
#531=PLANE('',#6147);
#532=PLANE('',#6148);
#533=PLANE('',#6149);
#534=PLANE('',#6150);
#819=FACE_OUTER_BOUND('',#1186,.T.);
#820=FACE_OUTER_BOUND('',#1187,.T.);
#821=FACE_OUTER_BOUND('',#1188,.T.);
#822=FACE_OUTER_BOUND('',#1189,.T.);
#823=FACE_OUTER_BOUND('',#1190,.T.);
#824=FACE_OUTER_BOUND('',#1191,.T.);
#825=FACE_OUTER_BOUND('',#1193,.T.);
#826=FACE_OUTER_BOUND('',#1195,.T.);
#827=FACE_OUTER_BOUND('',#1197,.T.);
#828=FACE_OUTER_BOUND('',#1198,.T.);
#829=FACE_OUTER_BOUND('',#1199,.T.);
#830=FACE_OUTER_BOUND('',#1200,.T.);
#831=FACE_OUTER_BOUND('',#1201,.T.);
#832=FACE_OUTER_BOUND('',#1202,.T.);
#833=FACE_OUTER_BOUND('',#1203,.T.);
#834=FACE_OUTER_BOUND('',#1204,.T.);
#835=FACE_OUTER_BOUND('',#1205,.T.);
#836=FACE_OUTER_BOUND('',#1206,.T.);
#837=FACE_OUTER_BOUND('',#1207,.T.);
#838=FACE_OUTER_BOUND('',#1208,.T.);
#839=FACE_OUTER_BOUND('',#1209,.T.);
#1186=EDGE_LOOP('',(#5005,#5006,#5007,#5008,#5009,#5010,#5011,#5012));
#1187=EDGE_LOOP('',(#5013,#5014,#5015,#5016));
#1188=EDGE_LOOP('',(#5017,#5018,#5019,#5020));
#1189=EDGE_LOOP('',(#5021,#5022,#5023,#5024));
#1190=EDGE_LOOP('',(#5025,#5026,#5027,#5028));
#1191=EDGE_LOOP('',(#5029));
#1192=EDGE_LOOP('',(#5030));
#1193=EDGE_LOOP('',(#5031));
#1194=EDGE_LOOP('',(#5032,#5033,#5034,#5035,#5036,#5037));
#1195=EDGE_LOOP('',(#5038));
#1196=EDGE_LOOP('',(#5039));
#1197=EDGE_LOOP('',(#5040));
#1198=EDGE_LOOP('',(#5041,#5042,#5043,#5044,#5045));
#1199=EDGE_LOOP('',(#5046,#5047,#5048,#5049,#5050));
#1200=EDGE_LOOP('',(#5051,#5052,#5053,#5054,#5055));
#1201=EDGE_LOOP('',(#5056,#5057,#5058,#5059,#5060));
#1202=EDGE_LOOP('',(#5061,#5062,#5063,#5064,#5065));
#1203=EDGE_LOOP('',(#5066,#5067,#5068,#5069,#5070));
#1204=EDGE_LOOP('',(#5071,#5072,#5073));
#1205=EDGE_LOOP('',(#5074,#5075,#5076));
#1206=EDGE_LOOP('',(#5077,#5078,#5079));
#1207=EDGE_LOOP('',(#5080,#5081,#5082));
#1208=EDGE_LOOP('',(#5083,#5084,#5085));
#1209=EDGE_LOOP('',(#5086,#5087,#5088));
#1635=LINE('',#12736,#2092);
#1636=LINE('',#12758,#2093);
#1637=LINE('',#12761,#2094);
#1638=LINE('',#12766,#2095);
#1639=LINE('',#12774,#2096);
#1640=LINE('',#12776,#2097);
#1641=LINE('',#12778,#2098);
#1642=LINE('',#12780,#2099);
#1643=LINE('',#12782,#2100);
#1644=LINE('',#12783,#2101);
#1645=LINE('',#12788,#2102);
#1646=LINE('',#12790,#2103);
#1647=LINE('',#12791,#2104);
#1648=LINE('',#12792,#2105);
#1649=LINE('',#12794,#2106);
#1650=LINE('',#12796,#2107);
#1651=LINE('',#12797,#2108);
#1652=LINE('',#12799,#2109);
#1653=LINE('',#12801,#2110);
#1654=LINE('',#12802,#2111);
#1655=LINE('',#12804,#2112);
#1656=LINE('',#12806,#2113);
#1657=LINE('',#12807,#2114);
#1658=LINE('',#12809,#2115);
#1659=LINE('',#12811,#2116);
#1660=LINE('',#12812,#2117);
#1661=LINE('',#12814,#2118);
#1662=LINE('',#12815,#2119);
#2092=VECTOR('',#7499,1732.05080756886);
#2093=VECTOR('',#7524,1.61);
#2094=VECTOR('',#7529,2.);
#2095=VECTOR('',#7534,3.8);
#2096=VECTOR('',#7543,1000.);
#2097=VECTOR('',#7544,1000.);
#2098=VECTOR('',#7545,1000.);
#2099=VECTOR('',#7546,1000.);
#2100=VECTOR('',#7547,1000.);
#2101=VECTOR('',#7548,1000.);
#2102=VECTOR('',#7555,1000.);
#2103=VECTOR('',#7556,1000.);
#2104=VECTOR('',#7557,1000.);
#2105=VECTOR('',#7558,1000.);
#2106=VECTOR('',#7561,1000.);
#2107=VECTOR('',#7562,1000.);
#2108=VECTOR('',#7563,1000.);
#2109=VECTOR('',#7566,1000.);
#2110=VECTOR('',#7567,1000.);
#2111=VECTOR('',#7568,1000.);
#2112=VECTOR('',#7571,1000.);
#2113=VECTOR('',#7572,1000.);
#2114=VECTOR('',#7573,1000.);
#2115=VECTOR('',#7576,1000.);
#2116=VECTOR('',#7577,1000.);
#2117=VECTOR('',#7578,1000.);
#2118=VECTOR('',#7581,1000.);
#2119=VECTOR('',#7582,1000.);
#2348=CIRCLE('',#6117,1.25);
#2349=CIRCLE('',#6118,1.25);
#2350=CIRCLE('',#6119,1.25);
#2351=CIRCLE('',#6120,1.25);
#2352=CIRCLE('',#6121,1.25);
#2353=CIRCLE('',#6122,1.25);
#2354=CIRCLE('',#6124,2.2);
#2355=CIRCLE('',#6125,0.2);
#2356=CIRCLE('',#6126,2.);
#2357=CIRCLE('',#6128,2.);
#2358=CIRCLE('',#6129,1.61);
#2359=CIRCLE('',#6132,3.8);
#2360=CIRCLE('',#6133,3.8);
#2361=CIRCLE('',#6135,1.9);
#2826=VERTEX_POINT('',#12734);
#2827=VERTEX_POINT('',#12735);
#2828=VERTEX_POINT('',#12737);
#2829=VERTEX_POINT('',#12739);
#2830=VERTEX_POINT('',#12741);
#2831=VERTEX_POINT('',#12743);
#2832=VERTEX_POINT('',#12745);
#2833=VERTEX_POINT('',#12749);
#2834=VERTEX_POINT('',#12751);
#2835=VERTEX_POINT('',#12755);
#2836=VERTEX_POINT('',#12757);
#2837=VERTEX_POINT('',#12763);
#2838=VERTEX_POINT('',#12765);
#2839=VERTEX_POINT('',#12769);
#2840=VERTEX_POINT('',#12772);
#2841=VERTEX_POINT('',#12773);
#2842=VERTEX_POINT('',#12775);
#2843=VERTEX_POINT('',#12777);
#2844=VERTEX_POINT('',#12779);
#2845=VERTEX_POINT('',#12781);
#2846=VERTEX_POINT('',#12787);
#2847=VERTEX_POINT('',#12789);
#2848=VERTEX_POINT('',#12795);
#2849=VERTEX_POINT('',#12800);
#2850=VERTEX_POINT('',#12805);
#2851=VERTEX_POINT('',#12810);
#3559=EDGE_CURVE('',#2826,#2827,#1635,.T.);
#3560=EDGE_CURVE('',#2827,#2828,#2348,.T.);
#3561=EDGE_CURVE('',#2828,#2829,#2349,.T.);
#3562=EDGE_CURVE('',#2829,#2830,#2350,.T.);
#3563=EDGE_CURVE('',#2830,#2831,#2351,.T.);
#3564=EDGE_CURVE('',#2831,#2832,#2352,.T.);
#3565=EDGE_CURVE('',#2832,#2827,#2353,.T.);
#3566=EDGE_CURVE('',#2833,#2833,#2354,.T.);
#3567=EDGE_CURVE('',#2833,#2834,#2355,.T.);
#3568=EDGE_CURVE('',#2834,#2834,#2356,.T.);
#3569=EDGE_CURVE('',#2835,#2835,#2357,.T.);
#3570=EDGE_CURVE('',#2835,#2836,#1636,.T.);
#3571=EDGE_CURVE('',#2836,#2836,#2358,.T.);
#3572=EDGE_CURVE('',#2834,#2835,#1637,.T.);
#3573=EDGE_CURVE('',#2837,#2837,#2359,.T.);
#3574=EDGE_CURVE('',#2837,#2838,#1638,.T.);
#3575=EDGE_CURVE('',#2838,#2838,#2360,.T.);
#3576=EDGE_CURVE('',#2839,#2839,#2361,.T.);
#3577=EDGE_CURVE('',#2840,#2841,#1639,.T.);
#3578=EDGE_CURVE('',#2841,#2842,#1640,.T.);
#3579=EDGE_CURVE('',#2842,#2843,#1641,.T.);
#3580=EDGE_CURVE('',#2843,#2844,#1642,.T.);
#3581=EDGE_CURVE('',#2844,#2845,#1643,.T.);
#3582=EDGE_CURVE('',#2845,#2840,#1644,.T.);
#3583=EDGE_CURVE('',#2846,#2829,#1645,.T.);
#3584=EDGE_CURVE('',#2829,#2847,#1646,.T.);
#3585=EDGE_CURVE('',#2847,#2842,#1647,.T.);
#3586=EDGE_CURVE('',#2846,#2841,#1648,.T.);
#3587=EDGE_CURVE('',#2847,#2828,#1649,.T.);
#3588=EDGE_CURVE('',#2828,#2848,#1650,.T.);
#3589=EDGE_CURVE('',#2848,#2843,#1651,.T.);
#3590=EDGE_CURVE('',#2848,#2827,#1652,.T.);
#3591=EDGE_CURVE('',#2827,#2849,#1653,.T.);
#3592=EDGE_CURVE('',#2849,#2844,#1654,.T.);
#3593=EDGE_CURVE('',#2849,#2832,#1655,.T.);
#3594=EDGE_CURVE('',#2832,#2850,#1656,.T.);
#3595=EDGE_CURVE('',#2850,#2845,#1657,.T.);
#3596=EDGE_CURVE('',#2850,#2831,#1658,.T.);
#3597=EDGE_CURVE('',#2831,#2851,#1659,.T.);
#3598=EDGE_CURVE('',#2851,#2840,#1660,.T.);
#3599=EDGE_CURVE('',#2851,#2830,#1661,.T.);
#3600=EDGE_CURVE('',#2830,#2846,#1662,.T.);
#5005=ORIENTED_EDGE('',*,*,#3559,.T.);
#5006=ORIENTED_EDGE('',*,*,#3560,.T.);
#5007=ORIENTED_EDGE('',*,*,#3561,.T.);
#5008=ORIENTED_EDGE('',*,*,#3562,.T.);
#5009=ORIENTED_EDGE('',*,*,#3563,.T.);
#5010=ORIENTED_EDGE('',*,*,#3564,.T.);
#5011=ORIENTED_EDGE('',*,*,#3565,.T.);
#5012=ORIENTED_EDGE('',*,*,#3559,.F.);
#5013=ORIENTED_EDGE('',*,*,#3566,.F.);
#5014=ORIENTED_EDGE('',*,*,#3567,.T.);
#5015=ORIENTED_EDGE('',*,*,#3568,.F.);
#5016=ORIENTED_EDGE('',*,*,#3567,.F.);
#5017=ORIENTED_EDGE('',*,*,#3569,.F.);
#5018=ORIENTED_EDGE('',*,*,#3570,.T.);
#5019=ORIENTED_EDGE('',*,*,#3571,.T.);
#5020=ORIENTED_EDGE('',*,*,#3570,.F.);
#5021=ORIENTED_EDGE('',*,*,#3568,.T.);
#5022=ORIENTED_EDGE('',*,*,#3572,.T.);
#5023=ORIENTED_EDGE('',*,*,#3569,.T.);
#5024=ORIENTED_EDGE('',*,*,#3572,.F.);
#5025=ORIENTED_EDGE('',*,*,#3573,.F.);
#5026=ORIENTED_EDGE('',*,*,#3574,.T.);
#5027=ORIENTED_EDGE('',*,*,#3575,.T.);
#5028=ORIENTED_EDGE('',*,*,#3574,.F.);
#5029=ORIENTED_EDGE('',*,*,#3573,.T.);
#5030=ORIENTED_EDGE('',*,*,#3576,.F.);
#5031=ORIENTED_EDGE('',*,*,#3576,.T.);
#5032=ORIENTED_EDGE('',*,*,#3577,.T.);
#5033=ORIENTED_EDGE('',*,*,#3578,.T.);
#5034=ORIENTED_EDGE('',*,*,#3579,.T.);
#5035=ORIENTED_EDGE('',*,*,#3580,.T.);
#5036=ORIENTED_EDGE('',*,*,#3581,.T.);
#5037=ORIENTED_EDGE('',*,*,#3582,.T.);
#5038=ORIENTED_EDGE('',*,*,#3575,.F.);
#5039=ORIENTED_EDGE('',*,*,#3566,.T.);
#5040=ORIENTED_EDGE('',*,*,#3571,.F.);
#5041=ORIENTED_EDGE('',*,*,#3583,.T.);
#5042=ORIENTED_EDGE('',*,*,#3584,.T.);
#5043=ORIENTED_EDGE('',*,*,#3585,.T.);
#5044=ORIENTED_EDGE('',*,*,#3578,.F.);
#5045=ORIENTED_EDGE('',*,*,#3586,.F.);
#5046=ORIENTED_EDGE('',*,*,#3587,.T.);
#5047=ORIENTED_EDGE('',*,*,#3588,.T.);
#5048=ORIENTED_EDGE('',*,*,#3589,.T.);
#5049=ORIENTED_EDGE('',*,*,#3579,.F.);
#5050=ORIENTED_EDGE('',*,*,#3585,.F.);
#5051=ORIENTED_EDGE('',*,*,#3590,.T.);
#5052=ORIENTED_EDGE('',*,*,#3591,.T.);
#5053=ORIENTED_EDGE('',*,*,#3592,.T.);
#5054=ORIENTED_EDGE('',*,*,#3580,.F.);
#5055=ORIENTED_EDGE('',*,*,#3589,.F.);
#5056=ORIENTED_EDGE('',*,*,#3593,.T.);
#5057=ORIENTED_EDGE('',*,*,#3594,.T.);
#5058=ORIENTED_EDGE('',*,*,#3595,.T.);
#5059=ORIENTED_EDGE('',*,*,#3581,.F.);
#5060=ORIENTED_EDGE('',*,*,#3592,.F.);
#5061=ORIENTED_EDGE('',*,*,#3596,.T.);
#5062=ORIENTED_EDGE('',*,*,#3597,.T.);
#5063=ORIENTED_EDGE('',*,*,#3598,.T.);
#5064=ORIENTED_EDGE('',*,*,#3582,.F.);
#5065=ORIENTED_EDGE('',*,*,#3595,.F.);
#5066=ORIENTED_EDGE('',*,*,#3599,.T.);
#5067=ORIENTED_EDGE('',*,*,#3600,.T.);
#5068=ORIENTED_EDGE('',*,*,#3586,.T.);
#5069=ORIENTED_EDGE('',*,*,#3577,.F.);
#5070=ORIENTED_EDGE('',*,*,#3598,.F.);
#5071=ORIENTED_EDGE('',*,*,#3565,.F.);
#5072=ORIENTED_EDGE('',*,*,#3593,.F.);
#5073=ORIENTED_EDGE('',*,*,#3591,.F.);
#5074=ORIENTED_EDGE('',*,*,#3564,.F.);
#5075=ORIENTED_EDGE('',*,*,#3596,.F.);
#5076=ORIENTED_EDGE('',*,*,#3594,.F.);
#5077=ORIENTED_EDGE('',*,*,#3563,.F.);
#5078=ORIENTED_EDGE('',*,*,#3599,.F.);
#5079=ORIENTED_EDGE('',*,*,#3597,.F.);
#5080=ORIENTED_EDGE('',*,*,#3562,.F.);
#5081=ORIENTED_EDGE('',*,*,#3583,.F.);
#5082=ORIENTED_EDGE('',*,*,#3600,.F.);
#5083=ORIENTED_EDGE('',*,*,#3561,.F.);
#5084=ORIENTED_EDGE('',*,*,#3587,.F.);
#5085=ORIENTED_EDGE('',*,*,#3584,.F.);
#5086=ORIENTED_EDGE('',*,*,#3560,.F.);
#5087=ORIENTED_EDGE('',*,*,#3590,.F.);
#5088=ORIENTED_EDGE('',*,*,#3588,.F.);
#5263=CYLINDRICAL_SURFACE('',#6130,2.);
#5264=CYLINDRICAL_SURFACE('',#6131,3.8);
#5536=ADVANCED_FACE('',(#819),#163,.F.);
#5537=ADVANCED_FACE('',(#820),#157,.F.);
#5538=ADVANCED_FACE('',(#821),#164,.T.);
#5539=ADVANCED_FACE('',(#822),#5263,.T.);
#5540=ADVANCED_FACE('',(#823),#5264,.T.);
#5541=ADVANCED_FACE('',(#824,#383),#153,.T.);
#5542=ADVANCED_FACE('',(#825,#384),#520,.T.);
#5543=ADVANCED_FACE('',(#826,#385),#521,.F.);
#5544=ADVANCED_FACE('',(#827),#522,.F.);
#5545=ADVANCED_FACE('',(#828),#523,.T.);
#5546=ADVANCED_FACE('',(#829),#524,.T.);
#5547=ADVANCED_FACE('',(#830),#525,.T.);
#5548=ADVANCED_FACE('',(#831),#526,.T.);
#5549=ADVANCED_FACE('',(#832),#527,.T.);
#5550=ADVANCED_FACE('',(#833),#528,.T.);
#5551=ADVANCED_FACE('',(#834),#529,.F.);
#5552=ADVANCED_FACE('',(#835),#530,.F.);
#5553=ADVANCED_FACE('',(#836),#531,.F.);
#5554=ADVANCED_FACE('',(#837),#532,.F.);
#5555=ADVANCED_FACE('',(#838),#533,.F.);
#5556=ADVANCED_FACE('',(#839),#534,.F.);
#5588=CLOSED_SHELL('',(#5536,#5537,#5538,#5539,#5540,#5541,#5542,#5543,
#5544,#5545,#5546,#5547,#5548,#5549,#5550,#5551,#5552,#5553,#5554,#5555,
#5556));
#6115=AXIS2_PLACEMENT_3D('',#12732,#7495,#7496);
#6116=AXIS2_PLACEMENT_3D('',#12733,#7497,#7498);
#6117=AXIS2_PLACEMENT_3D('',#12738,#7500,#7501);
#6118=AXIS2_PLACEMENT_3D('',#12740,#7502,#7503);
#6119=AXIS2_PLACEMENT_3D('',#12742,#7504,#7505);
#6120=AXIS2_PLACEMENT_3D('',#12744,#7506,#7507);
#6121=AXIS2_PLACEMENT_3D('',#12746,#7508,#7509);
#6122=AXIS2_PLACEMENT_3D('',#12747,#7510,#7511);
#6123=AXIS2_PLACEMENT_3D('',#12748,#7512,#7513);
#6124=AXIS2_PLACEMENT_3D('',#12750,#7514,#7515);
#6125=AXIS2_PLACEMENT_3D('',#12752,#7516,#7517);
#6126=AXIS2_PLACEMENT_3D('',#12753,#7518,#7519);
#6127=AXIS2_PLACEMENT_3D('',#12754,#7520,#7521);
#6128=AXIS2_PLACEMENT_3D('',#12756,#7522,#7523);
#6129=AXIS2_PLACEMENT_3D('',#12759,#7525,#7526);
#6130=AXIS2_PLACEMENT_3D('',#12760,#7527,#7528);
#6131=AXIS2_PLACEMENT_3D('',#12762,#7530,#7531);
#6132=AXIS2_PLACEMENT_3D('',#12764,#7532,#7533);
#6133=AXIS2_PLACEMENT_3D('',#12767,#7535,#7536);
#6134=AXIS2_PLACEMENT_3D('',#12768,#7537,#7538);
#6135=AXIS2_PLACEMENT_3D('',#12770,#7539,#7540);
#6136=AXIS2_PLACEMENT_3D('',#12771,#7541,#7542);
#6137=AXIS2_PLACEMENT_3D('',#12784,#7549,#7550);
#6138=AXIS2_PLACEMENT_3D('',#12785,#7551,#7552);
#6139=AXIS2_PLACEMENT_3D('',#12786,#7553,#7554);
#6140=AXIS2_PLACEMENT_3D('',#12793,#7559,#7560);
#6141=AXIS2_PLACEMENT_3D('',#12798,#7564,#7565);
#6142=AXIS2_PLACEMENT_3D('',#12803,#7569,#7570);
#6143=AXIS2_PLACEMENT_3D('',#12808,#7574,#7575);
#6144=AXIS2_PLACEMENT_3D('',#12813,#7579,#7580);
#6145=AXIS2_PLACEMENT_3D('',#12816,#7583,#7584);
#6146=AXIS2_PLACEMENT_3D('',#12817,#7585,#7586);
#6147=AXIS2_PLACEMENT_3D('',#12818,#7587,#7588);
#6148=AXIS2_PLACEMENT_3D('',#12819,#7589,#7590);
#6149=AXIS2_PLACEMENT_3D('',#12820,#7591,#7592);
#6150=AXIS2_PLACEMENT_3D('',#12821,#7593,#7594);
#7495=DIRECTION('axis',(0.,0.,1.));
#7496=DIRECTION('refdir',(1.,0.,0.));
#7497=DIRECTION('center_axis',(-1.,0.,0.));
#7498=DIRECTION('ref_axis',(0.,0.,1.));
#7499=DIRECTION('',(-0.500000000000004,-1.0605752387249E-16,-0.866025403784436));
#7500=DIRECTION('center_axis',(-1.,0.,0.));
#7501=DIRECTION('ref_axis',(0.,0.,1.));
#7502=DIRECTION('center_axis',(-1.,0.,0.));
#7503=DIRECTION('ref_axis',(0.,0.,1.));
#7504=DIRECTION('center_axis',(-1.,0.,0.));
#7505=DIRECTION('ref_axis',(0.,0.,1.));
#7506=DIRECTION('center_axis',(-1.,0.,0.));
#7507=DIRECTION('ref_axis',(0.,0.,1.));
#7508=DIRECTION('center_axis',(-1.,0.,0.));
#7509=DIRECTION('ref_axis',(0.,0.,1.));
#7510=DIRECTION('center_axis',(-1.,0.,0.));
#7511=DIRECTION('ref_axis',(0.,0.,1.));
#7512=DIRECTION('center_axis',(-1.,0.,0.));
#7513=DIRECTION('ref_axis',(0.,0.,1.));
#7514=DIRECTION('center_axis',(-1.,0.,0.));
#7515=DIRECTION('ref_axis',(0.,0.,1.));
#7516=DIRECTION('center_axis',(0.,1.,-1.22464679914735E-16));
#7517=DIRECTION('ref_axis',(0.,-1.22464679914735E-16,-1.));
#7518=DIRECTION('center_axis',(1.,0.,0.));
#7519=DIRECTION('ref_axis',(0.,0.,1.));
#7520=DIRECTION('center_axis',(-1.,0.,0.));
#7521=DIRECTION('ref_axis',(0.,0.,1.));
#7522=DIRECTION('center_axis',(-1.,0.,0.));
#7523=DIRECTION('ref_axis',(0.,0.,1.));
#7524=DIRECTION('',(0.707106781186548,8.65956056235492E-17,0.707106781186547));
#7525=DIRECTION('center_axis',(-1.,0.,0.));
#7526=DIRECTION('ref_axis',(0.,0.,1.));
#7527=DIRECTION('center_axis',(-1.,0.,0.));
#7528=DIRECTION('ref_axis',(0.,0.,1.));
#7529=DIRECTION('',(1.,0.,0.));
#7530=DIRECTION('center_axis',(-1.,0.,0.));
#7531=DIRECTION('ref_axis',(0.,0.,1.));
#7532=DIRECTION('center_axis',(-1.,0.,0.));
#7533=DIRECTION('ref_axis',(0.,0.,1.));
#7534=DIRECTION('',(1.,0.,0.));
#7535=DIRECTION('center_axis',(-1.,0.,0.));
#7536=DIRECTION('ref_axis',(0.,0.,1.));
#7537=DIRECTION('center_axis',(0.,6.12323399573677E-17,-1.));
#7538=DIRECTION('ref_axis',(0.,1.,0.));
#7539=DIRECTION('center_axis',(-1.,0.,0.));
#7540=DIRECTION('ref_axis',(0.,0.,1.));
#7541=DIRECTION('center_axis',(-1.,0.,0.));
#7542=DIRECTION('ref_axis',(0.,0.,1.));
#7543=DIRECTION('',(0.,-1.,1.50231459873716E-16));
#7544=DIRECTION('',(0.,-0.5,-0.866025403784438));
#7545=DIRECTION('',(0.,0.5,-0.866025403784438));
#7546=DIRECTION('',(0.,1.,0.));
#7547=DIRECTION('',(0.,0.5,0.866025403784438));
#7548=DIRECTION('',(0.,-0.5,0.866025403784438));
#7549=DIRECTION('center_axis',(-1.,0.,0.));
#7550=DIRECTION('ref_axis',(0.,0.,1.));
#7551=DIRECTION('center_axis',(-1.,0.,0.));
#7552=DIRECTION('ref_axis',(0.,0.,1.));
#7553=DIRECTION('center_axis',(0.,0.866025403784438,-0.5));
#7554=DIRECTION('ref_axis',(0.,0.5,0.866025403784438));
#7555=DIRECTION('',(0.,-0.5,-0.866025403784438));
#7556=DIRECTION('',(0.,-0.5,-0.866025403784438));
#7557=DIRECTION('',(-1.,0.,0.));
#7558=DIRECTION('',(-1.,0.,0.));
#7559=DIRECTION('center_axis',(0.,0.866025403784438,0.5));
#7560=DIRECTION('ref_axis',(0.,-0.5,0.866025403784438));
#7561=DIRECTION('',(0.,0.5,-0.866025403784438));
#7562=DIRECTION('',(0.,0.5,-0.866025403784438));
#7563=DIRECTION('',(-1.,0.,0.));
#7564=DIRECTION('center_axis',(0.,0.,1.));
#7565=DIRECTION('ref_axis',(1.,0.,0.));
#7566=DIRECTION('',(0.,1.,0.));
#7567=DIRECTION('',(0.,1.,0.));
#7568=DIRECTION('',(-1.,0.,0.));
#7569=DIRECTION('center_axis',(0.,-0.866025403784439,0.5));
#7570=DIRECTION('ref_axis',(0.,-0.5,-0.866025403784439));
#7571=DIRECTION('',(0.,0.5,0.866025403784438));
#7572=DIRECTION('',(0.,0.5,0.866025403784438));
#7573=DIRECTION('',(-1.,0.,0.));
#7574=DIRECTION('center_axis',(0.,-0.866025403784439,-0.5));
#7575=DIRECTION('ref_axis',(0.,0.5,-0.866025403784439));
#7576=DIRECTION('',(0.,-0.5,0.866025403784438));
#7577=DIRECTION('',(0.,-0.5,0.866025403784438));
#7578=DIRECTION('',(-1.,0.,0.));
#7579=DIRECTION('center_axis',(0.,-1.50231459873716E-16,-1.));
#7580=DIRECTION('ref_axis',(0.,1.,-1.50231459873716E-16));
#7581=DIRECTION('',(0.,-1.,1.50231459873716E-16));
#7582=DIRECTION('',(0.,-1.,1.50231459873716E-16));
#7583=DIRECTION('center_axis',(1.,0.,0.));
#7584=DIRECTION('ref_axis',(0.,0.,-1.));
#7585=DIRECTION('center_axis',(1.,0.,0.));
#7586=DIRECTION('ref_axis',(0.,0.,-1.));
#7587=DIRECTION('center_axis',(1.,0.,0.));
#7588=DIRECTION('ref_axis',(0.,0.,-1.));
#7589=DIRECTION('center_axis',(1.,0.,0.));
#7590=DIRECTION('ref_axis',(0.,0.,-1.));
#7591=DIRECTION('center_axis',(1.,0.,0.));
#7592=DIRECTION('ref_axis',(0.,0.,-1.));
#7593=DIRECTION('center_axis',(1.,0.,0.));
#7594=DIRECTION('ref_axis',(0.,0.,-1.));
#12732=CARTESIAN_POINT('',(0.,0.,0.));
#12733=CARTESIAN_POINT('Origin',(-997.978312163513,0.,0.));
#12734=CARTESIAN_POINT('',(2.02168783648704,2.16840434497101E-16,0.));
#12735=CARTESIAN_POINT('',(1.3,0.,-1.25));
#12736=CARTESIAN_POINT('',(-997.978312163513,-2.12115047744979E-13,-1732.05080756886));
#12737=CARTESIAN_POINT('',(1.3,-1.08253175473055,-0.625000000000001));
#12738=CARTESIAN_POINT('Origin',(1.3,0.,0.));
#12739=CARTESIAN_POINT('',(1.3,-1.08253175473055,0.625));
#12740=CARTESIAN_POINT('Origin',(1.3,0.,0.));
#12741=CARTESIAN_POINT('',(1.3,1.87789324842145E-16,1.25));
#12742=CARTESIAN_POINT('Origin',(1.3,0.,0.));
#12743=CARTESIAN_POINT('',(1.3,1.08253175473055,0.625000000000001));
#12744=CARTESIAN_POINT('Origin',(1.3,0.,0.));
#12745=CARTESIAN_POINT('',(1.3,1.08253175473055,-0.625));
#12746=CARTESIAN_POINT('Origin',(1.3,0.,0.));
#12747=CARTESIAN_POINT('Origin',(1.3,0.,0.));
#12748=CARTESIAN_POINT('Origin',(2.4,0.,0.));
#12749=CARTESIAN_POINT('',(2.2,-2.69422295812418E-16,-2.2));
#12750=CARTESIAN_POINT('Origin',(2.2,0.,0.));
#12751=CARTESIAN_POINT('',(2.4,-2.44929359829471E-16,-2.));
#12752=CARTESIAN_POINT('Origin',(2.4,-2.69422295812418E-16,-2.2));
#12753=CARTESIAN_POINT('Origin',(2.4,0.,0.));
#12754=CARTESIAN_POINT('Origin',(6.2,0.,0.));
#12755=CARTESIAN_POINT('',(5.81,-2.44929359829471E-16,-2.));
#12756=CARTESIAN_POINT('Origin',(5.81,0.,0.));
#12757=CARTESIAN_POINT('',(6.2,-1.97168134662724E-16,-1.61));
#12758=CARTESIAN_POINT('',(6.2,-1.97168134662724E-16,-1.61));
#12759=CARTESIAN_POINT('Origin',(6.2,0.,0.));
#12760=CARTESIAN_POINT('Origin',(0.,0.,0.));
#12761=CARTESIAN_POINT('',(0.,-2.44929359829471E-16,-2.));
#12762=CARTESIAN_POINT('Origin',(0.,0.,0.));
#12763=CARTESIAN_POINT('',(1.82,-4.65365783675994E-16,-3.8));
#12764=CARTESIAN_POINT('Origin',(1.82,0.,0.));
#12765=CARTESIAN_POINT('',(2.2,-4.65365783675994E-16,-3.8));
#12766=CARTESIAN_POINT('',(0.,-4.65365783675994E-16,-3.8));
#12767=CARTESIAN_POINT('Origin',(2.2,0.,0.));
#12768=CARTESIAN_POINT('Origin',(3.88527472527473,-4.33680868994202E-16,
0.));
#12769=CARTESIAN_POINT('',(4.33680868994202E-16,1.9,0.));
#12770=CARTESIAN_POINT('Origin',(4.33680868994202E-16,0.,0.));
#12771=CARTESIAN_POINT('Origin',(2.16840434497101E-16,0.,0.));
#12772=CARTESIAN_POINT('',(0.,0.721687836487033,1.25));
#12773=CARTESIAN_POINT('',(2.16840434497101E-16,-0.721687836487032,1.25));
#12774=CARTESIAN_POINT('',(0.,-0.721687836487032,1.25));
#12775=CARTESIAN_POINT('',(0.,-1.44337567297406,3.94456587164721E-18));
#12776=CARTESIAN_POINT('',(0.,-1.44337567297406,3.94456587164721E-18));
#12777=CARTESIAN_POINT('',(0.,-0.721687836487032,-1.25));
#12778=CARTESIAN_POINT('',(0.,-0.721687836487032,-1.25));
#12779=CARTESIAN_POINT('',(0.,0.721687836487033,-1.25));
#12780=CARTESIAN_POINT('',(0.,0.721687836487033,-1.25));
#12781=CARTESIAN_POINT('',(0.,1.44337567297407,-1.08420217247849E-16));
#12782=CARTESIAN_POINT('',(0.,1.44337567297407,-1.08420217247849E-16));
#12783=CARTESIAN_POINT('',(0.,0.721687836487033,1.25));
#12784=CARTESIAN_POINT('Origin',(2.2,2.,0.));
#12785=CARTESIAN_POINT('Origin',(6.2,0.,0.));
#12786=CARTESIAN_POINT('Origin',(1.3,-1.44337567297406,3.94456587164721E-18));
#12787=CARTESIAN_POINT('',(1.3,-0.721687836487032,1.25));
#12788=CARTESIAN_POINT('',(1.3,-1.44337567297406,3.94456587164721E-18));
#12789=CARTESIAN_POINT('',(1.3,-1.44337567297406,3.94456587164721E-18));
#12790=CARTESIAN_POINT('',(1.3,-1.44337567297406,3.94456587164721E-18));
#12791=CARTESIAN_POINT('',(1.3,-1.44337567297406,3.94456587164721E-18));
#12792=CARTESIAN_POINT('',(1.3,-0.721687836487032,1.25));
#12793=CARTESIAN_POINT('Origin',(1.3,-0.721687836487032,-1.25));
#12794=CARTESIAN_POINT('',(1.3,-0.721687836487032,-1.25));
#12795=CARTESIAN_POINT('',(1.3,-0.721687836487032,-1.25));
#12796=CARTESIAN_POINT('',(1.3,-0.721687836487032,-1.25));
#12797=CARTESIAN_POINT('',(1.3,-0.721687836487032,-1.25));
#12798=CARTESIAN_POINT('Origin',(1.3,0.721687836487033,-1.25));
#12799=CARTESIAN_POINT('',(1.3,0.721687836487033,-1.25));
#12800=CARTESIAN_POINT('',(1.3,0.721687836487033,-1.25));
#12801=CARTESIAN_POINT('',(1.3,0.721687836487033,-1.25));
#12802=CARTESIAN_POINT('',(1.3,0.721687836487033,-1.25));
#12803=CARTESIAN_POINT('Origin',(1.3,1.44337567297407,-1.08420217247849E-16));
#12804=CARTESIAN_POINT('',(1.3,1.44337567297407,-1.08420217247849E-16));
#12805=CARTESIAN_POINT('',(1.3,1.44337567297407,-1.08420217247849E-16));
#12806=CARTESIAN_POINT('',(1.3,1.44337567297407,-1.08420217247849E-16));
#12807=CARTESIAN_POINT('',(1.3,1.44337567297407,-1.08420217247849E-16));
#12808=CARTESIAN_POINT('Origin',(1.3,0.721687836487033,1.25));
#12809=CARTESIAN_POINT('',(1.3,0.721687836487033,1.25));
#12810=CARTESIAN_POINT('',(1.3,0.721687836487033,1.25));
#12811=CARTESIAN_POINT('',(1.3,0.721687836487033,1.25));
#12812=CARTESIAN_POINT('',(1.3,0.721687836487033,1.25));
#12813=CARTESIAN_POINT('Origin',(1.3,-0.721687836487032,1.25));
#12814=CARTESIAN_POINT('',(1.3,-0.721687836487032,1.25));
#12815=CARTESIAN_POINT('',(1.3,-0.721687836487032,1.25));
#12816=CARTESIAN_POINT('Origin',(1.3,-1.44337567297406,-2.16840434497101E-16));
#12817=CARTESIAN_POINT('Origin',(1.3,-1.44337567297406,-2.16840434497101E-16));
#12818=CARTESIAN_POINT('Origin',(1.3,-1.44337567297406,-2.16840434497101E-16));
#12819=CARTESIAN_POINT('Origin',(1.3,-1.44337567297406,-2.16840434497101E-16));
#12820=CARTESIAN_POINT('Origin',(1.3,-1.44337567297406,-2.16840434497101E-16));
#12821=CARTESIAN_POINT('Origin',(1.3,-1.44337567297406,-2.16840434497101E-16));
#12954=UNCERTAINTY_MEASURE_WITH_UNIT(LENGTH_MEASURE(0.01),#12967,
'DISTANCE_ACCURACY_VALUE',
'Maximum model space distance between geometric entities at asserted c
onnectivities');
#12956=UNCERTAINTY_MEASURE_WITH_UNIT(LENGTH_MEASURE(0.01),#12967,
'DISTANCE_ACCURACY_VALUE',
'Maximum model space distance between geometric entities at asserted c
onnectivities');
#12964=(
GEOMETRIC_REPRESENTATION_CONTEXT(3)
GLOBAL_UNCERTAINTY_ASSIGNED_CONTEXT((#12954))
GLOBAL_UNIT_ASSIGNED_CONTEXT((#12967,#12969,#12970))
REPRESENTATION_CONTEXT('','3D')
);
#12966=(
GEOMETRIC_REPRESENTATION_CONTEXT(3)
GLOBAL_UNCERTAINTY_ASSIGNED_CONTEXT((#12956))
GLOBAL_UNIT_ASSIGNED_CONTEXT((#12967,#12969,#12970))
REPRESENTATION_CONTEXT('','3D')
);
#12967=(
LENGTH_UNIT()
NAMED_UNIT(*)
SI_UNIT(.MILLI.,.METRE.)
);
#12969=(
NAMED_UNIT(*)
PLANE_ANGLE_UNIT()
SI_UNIT($,.RADIAN.)
);
#12970=(
NAMED_UNIT(*)
SI_UNIT($,.STERADIAN.)
SOLID_ANGLE_UNIT()
);
#12978=SHAPE_DEFINITION_REPRESENTATION(#12987,#13031);
#12987=PRODUCT_DEFINITION_SHAPE('',$,#13041);
#13031=SHAPE_REPRESENTATION('',(#6115),#12964);
#13033=PRODUCT_DEFINITION_CONTEXT('part definition',#13062,'design');
#13041=PRODUCT_DEFINITION('Button Head Cap Screw M4x0.7x4',
'Button Head Cap Screw M4x0.7x4',#13050,#13033);
#13050=PRODUCT_DEFINITION_FORMATION('',$,#13071);
#13062=APPLICATION_CONTEXT(
'Core Data for Automotive Mechanical Design Process');
#13063=PRODUCT_CONTEXT('part definition',#13062,'mechanical');
#13071=PRODUCT('Button Head Cap Screw M4x0.7x4',
'Button Head Cap Screw M4x0.7x4',$,(#13063));
#13075=PRESENTATION_STYLE_ASSIGNMENT((#13080));
#13080=SURFACE_STYLE_USAGE(.BOTH.,#13085);
#13085=SURFACE_SIDE_STYLE('',(#13090));
#13090=SURFACE_STYLE_FILL_AREA(#13095);
#13095=FILL_AREA_STYLE('Opaque(31,36,43)',(#13100));
#13100=FILL_AREA_STYLE_COLOUR('Opaque(31,36,43)',#13105);
#13105=COLOUR_RGB('Opaque(31,36,43)',0.12156862745098,0.141176470588235,
0.168627450980392);
ENDSEC;
END-ISO-10303-21;
